ISO-10303-21;
HEADER;
FILE_DESCRIPTION (('STEP AP214'),
    '1' );
FILE_NAME ('socket head cap screw_iso_ISO 4762 M3 x 8 - 8N.step',
    '2026-10-03T18:28:46',
    ( '' ),
    ( '' ),
    'SwSTEP 2.0',
    'SolidWorks 2026',
    '' );
FILE_SCHEMA (( 'AUTOMOTIVE_DESIGN' ));
ENDSEC;

DATA;
#6=CARTESIAN_POINT ( 'NONE',  ( 10.71950000000001424, 0.000000000000000000, 1.500000000000000222 ) ) ;
#15=DIRECTION ( 'NONE',  ( 0.000000000000000000, 1.000000000000000000, -1.320393690296331133E-15 ) ) ;
#29=DIRECTION ( 'NONE',  ( -1.000000000000000000, -0.000000000000000000, -0.000000000000000000 ) ) ;
#39=ORIENTED_EDGE ( 'NONE', *, *, #10148, .F. ) ;
#54=APPLICATION_CONTEXT ( 'automotive_design' ) ;
#56=PRODUCT ( 'socket head cap screw_iso_ISO 4762 M3 x 8 - 8N', 'socket head cap screw_iso_ISO 4762 M3 x 8 - 8N', '', ( #8757 ) ) ;
#65=VERTEX_POINT ( 'NONE', #8189 ) ;
#69=ADVANCED_FACE ( 'NONE', ( #9627 ), #4044, .F. ) ;
#75=DIRECTION ( 'NONE',  ( 1.000000000000000000, 0.000000000000000000, 0.000000000000000000 ) ) ;
#77=SURFACE_STYLE_FILL_AREA ( #6636 ) ;
#84=ORIENTED_EDGE ( 'NONE', *, *, #6223, .T. ) ;
#94=ADVANCED_FACE ( 'NONE', ( #8824 ), #10482, .F. ) ;
#121=CARTESIAN_POINT ( 'NONE',  ( 1.300000000000000044, -0.7390083445627200209, 1.280000000000001137 ) ) ;
#136=FACE_OUTER_BOUND ( 'NONE', #5788, .T. ) ;
#162=LINE ( 'NONE', #5033, #9824 ) ;
#165=VERTEX_POINT ( 'NONE', #5934 ) ;
#176=LINE ( 'NONE', #3458, #275 ) ;
#179=CARTESIAN_POINT ( 'NONE',  ( 1.300000000000000044, 0.000000000000000000, 0.000000000000000000 ) ) ;
#191=CARTESIAN_POINT ( 'NONE',  ( 1.300000000000000044, -1.108512516844081475, 0.6400000000000016787 ) ) ;
#251=( LENGTH_UNIT ( ) NAMED_UNIT ( * ) SI_UNIT ( .MILLI., .METRE. ) );
#275=VECTOR ( 'NONE', #4885, 1000.000000000000000 ) ;
#284=DIRECTION ( 'NONE',  ( -1.000000000000000000, -0.000000000000000000, -0.000000000000000000 ) ) ;
#319=FACE_OUTER_BOUND ( 'NONE', #4764, .T. ) ;
#324=CIRCLE ( 'NONE', #7596, 1.280000000000000027 ) ;
#326=DIRECTION ( 'NONE',  ( 0.000000000000000000, 0.000000000000000000, -1.000000000000000000 ) ) ;
#354=VECTOR ( 'NONE', #1516, 1000.000000000000000 ) ;
#356=DIRECTION ( 'NONE',  ( 0.000000000000000000, 0.000000000000000000, 1.000000000000000000 ) ) ;
#357=AXIS2_PLACEMENT_3D ( 'NONE', #179, #3413, #5576 ) ;
#358=DIRECTION ( 'NONE',  ( 0.000000000000000000, 0.000000000000000000, 1.000000000000000000 ) ) ;
#359=ORIENTED_EDGE ( 'NONE', *, *, #10190, .F. ) ;
#362=CIRCLE ( 'NONE', #3066, 1.500000000000000222 ) ;
#368=CARTESIAN_POINT ( 'NONE',  ( 3.099999999999998757, 1.836970198721030181E-16, -1.500000000000000222 ) ) ;
#404=ORIENTED_EDGE ( 'NONE', *, *, #8112, .F. ) ;
#418=ORIENTED_EDGE ( 'NONE', *, *, #480, .T. ) ;
#432=FACE_OUTER_BOUND ( 'NONE', #1916, .T. ) ;
#444=CARTESIAN_POINT ( 'NONE',  ( 1.300000000000000044, -1.478016689125442706, 1.843143693225357538E-15 ) ) ;
#448=CARTESIAN_POINT ( 'NONE',  ( 1.300000000000000044, 1.478016689125442484, -1.626303258728256651E-15 ) ) ;
#454=ORIENTED_EDGE ( 'NONE', *, *, #1956, .T. ) ;
#474=DIRECTION ( 'NONE',  ( 0.000000000000000000, 0.000000000000000000, -1.000000000000000000 ) ) ;
#480=EDGE_CURVE ( 'NONE', #4172, #5208, #324, .T. ) ;
#494=CARTESIAN_POINT ( 'NONE',  ( 3.000000000000000888, 0.000000000000000000, 0.000000000000000000 ) ) ;
#495=DIRECTION ( 'NONE',  ( 0.000000000000000000, -0.5000000000000013323, -0.8660254037844378194 ) ) ;
#500=EDGE_LOOP ( 'NONE', ( #2992, #7233 ) ) ;
#510=CIRCLE ( 'NONE', #10175, 0.1499999999999999667 ) ;
#520=VERTEX_POINT ( 'NONE', #5255 ) ;
#532=AXIS2_PLACEMENT_3D ( 'NONE', #7551, #3468, #3418 ) ;
#557=CARTESIAN_POINT ( 'NONE',  ( 11.00000000000000355, 0.000000000000000000, 1.219500000000000028 ) ) ;
#583=CYLINDRICAL_SURFACE ( 'NONE', #1539, 2.750000000000000000 ) ;
#592=CIRCLE ( 'NONE', #5335, 1.280000000000000027 ) ;
#595=EDGE_CURVE ( 'NONE', #8537, #2545, #5893, .T. ) ;
#603=DIRECTION ( 'NONE',  ( 0.000000000000000000, -0.8660254037844391517, -0.4999999999999992784 ) ) ;
#623=DIRECTION ( 'NONE',  ( -1.000000000000000000, -0.000000000000000000, -0.000000000000000000 ) ) ;
#627=DIRECTION ( 'NONE',  ( 1.000000000000000000, 0.000000000000000000, 0.000000000000000000 ) ) ;
#633=CARTESIAN_POINT ( 'NONE',  ( 1.300000000000000044, 0.000000000000000000, 0.000000000000000000 ) ) ;
#654=EDGE_CURVE ( 'NONE', #729, #8371, #1490, .T. ) ;
#667=ORIENTED_EDGE ( 'NONE', *, *, #7014, .F. ) ;
#675=VECTOR ( 'NONE', #8846, 1000.000000000000000 ) ;
#697=VECTOR ( 'NONE', #5045, 1000.000000000000114 ) ;
#698=DIRECTION ( 'NONE',  ( -1.000000000000000000, -0.000000000000000000, -0.000000000000000000 ) ) ;
#704=ORIENTED_EDGE ( 'NONE', *, *, #9980, .F. ) ;
#721=EDGE_CURVE ( 'NONE', #3971, #3139, #8290, .T. ) ;
#725=CARTESIAN_POINT ( 'NONE',  ( 0.000000000000000000, 0.000000000000000000, 0.000000000000000000 ) ) ;
#729=VERTEX_POINT ( 'NONE', #10467 ) ;
#734=EDGE_CURVE ( 'NONE', #7181, #6113, #8913, .T. ) ;
#743=ORIENTED_EDGE ( 'NONE', *, *, #734, .F. ) ;
#756=DIRECTION ( 'NONE',  ( -1.000000000000000000, -0.000000000000000000, -0.000000000000000000 ) ) ;
#763=CARTESIAN_POINT ( 'NONE',  ( 1.300000000000000044, 1.478016689125442484, -1.626303258728256651E-15 ) ) ;
#783=AXIS2_PLACEMENT_3D ( 'NONE', #9681, #8871, #7111 ) ;
#786=DIRECTION ( 'NONE',  ( 0.000000000000000000, -1.000000000000000000, 1.026972870230479989E-15 ) ) ;
#787=EDGE_CURVE ( 'NONE', #8703, #2420, #2314, .T. ) ;
#798=VERTEX_POINT ( 'NONE', #4633 ) ;
#811=DIRECTION ( 'NONE',  ( 1.000000000000000000, 0.000000000000000000, 0.000000000000000000 ) ) ;
#813=DIRECTION ( 'NONE',  ( -1.000000000000000000, -0.000000000000000000, -0.000000000000000000 ) ) ;
#824=ORIENTED_EDGE ( 'NONE', *, *, #3871, .F. ) ;
#835=AXIS2_PLACEMENT_3D ( 'NONE', #8806, #698, #3239 ) ;
#840=CARTESIAN_POINT ( 'NONE',  ( 11.00000000000000355, 1.219500000000000028, 0.000000000000000000 ) ) ;
#853=CIRCLE ( 'NONE', #3726, 2.600000000000000089 ) ;
#868=DIRECTION ( 'NONE',  ( 0.000000000000000000, 0.4999999999999991673, -0.8660254037844391517 ) ) ;
#888=ORIENTED_EDGE ( 'NONE', *, *, #8564, .F. ) ;
#899=ADVANCED_FACE ( 'NONE', ( #10134 ), #10152, .F. ) ;
#920=FILL_AREA_STYLE_COLOUR ( '', #1541 ) ;
#941=( NAMED_UNIT ( * ) SI_UNIT ( $, .STERADIAN. ) SOLID_ANGLE_UNIT ( ) );
#1008=EDGE_LOOP ( 'NONE', ( #7813, #4123, #3488 ) ) ;
#1044=FILL_AREA_STYLE ('',( #6051 ) ) ;
#1073=CYLINDRICAL_SURFACE ( 'NONE', #2483, 1.500000000000000222 ) ;
#1078=CIRCLE ( 'NONE', #3283, 1.280000000000000027 ) ;
#1090=ORIENTED_EDGE ( 'NONE', *, *, #595, .T. ) ;
#1091=( NAMED_UNIT ( * ) PLANE_ANGLE_UNIT ( ) SI_UNIT ( $, .RADIAN. ) );
#1104=( GEOMETRIC_REPRESENTATION_CONTEXT ( 3 ) GLOBAL_UNCERTAINTY_ASSIGNED_CONTEXT ( ( #2307 ) ) GLOBAL_UNIT_ASSIGNED_CONTEXT ( ( #2584, #9704, #941 ) ) REPRESENTATION_CONTEXT ( 'NONE', 'WORKASPACE' ) );
#1111=CARTESIAN_POINT ( 'NONE',  ( 1.300000000000000044, -0.7390083445627225744, -1.279999999999999138 ) ) ;
#1120=PLANE ( 'NONE',  #1762 ) ;
#1125=DIRECTION ( 'NONE',  ( 0.000000000000000000, 0.000000000000000000, 1.000000000000000000 ) ) ;
#1162=ORIENTED_EDGE ( 'NONE', *, *, #787, .F. ) ;
#1186=ORIENTED_EDGE ( 'NONE', *, *, #1304, .T. ) ;
#1208=DIRECTION ( 'NONE',  ( -0.000000000000000000, 0.000000000000000000, 1.000000000000000000 ) ) ;
#1216=PLANE ( 'NONE',  #6136 ) ;
#1236=MANIFOLD_SOLID_BREP ( 'Hex', #1694 ) ;
#1245=ADVANCED_FACE ( 'NONE', ( #3200 ), #8245, .F. ) ;
#1260=EDGE_CURVE ( 'NONE', #798, #4172, #4077, .T. ) ;
#1288=DIRECTION ( 'NONE',  ( -0.7071067811865335839, 0.000000000000000000, 0.7071067811865614505 ) ) ;
#1304=EDGE_CURVE ( 'NONE', #5208, #8945, #5835, .T. ) ;
#1310=EDGE_LOOP ( 'NONE', ( #2242, #7691, #7079, #9739 ) ) ;
#1333=VECTOR ( 'NONE', #9587, 1000.000000000000000 ) ;
#1374=VECTOR ( 'NONE', #2108, 1000.000000000000227 ) ;
#1403=CARTESIAN_POINT ( 'NONE',  ( 0.000000000000000000, 0.7390083445627224634, 1.279999999999999138 ) ) ;
#1430=DIRECTION ( 'NONE',  ( 0.000000000000000000, 0.000000000000000000, 1.000000000000000000 ) ) ;
#1434=DIRECTION ( 'NONE',  ( -1.000000000000000000, -0.000000000000000000, -0.000000000000000000 ) ) ;
#1442=ORIENTED_EDGE ( 'NONE', *, *, #2860, .T. ) ;
#1445=CARTESIAN_POINT ( 'NONE',  ( 11.00000000000000355, 0.000000000000000000, 0.000000000000000000 ) ) ;
#1455=UNCERTAINTY_MEASURE_WITH_UNIT (LENGTH_MEASURE( 1.000000000000000082E-05 ), #7334, 'distance_accuracy_value', 'NONE');
#1458=AXIS2_PLACEMENT_3D ( 'NONE', #7318, #7211, #7096 ) ;
#1472=DIRECTION ( 'NONE',  ( -1.000000000000000000, -0.000000000000000000, -0.000000000000000000 ) ) ;
#1490=LINE ( 'NONE', #6360, #10314 ) ;
#1516=DIRECTION ( 'NONE',  ( 0.000000000000000000, -0.4999999999999992784, 0.8660254037844390407 ) ) ;
#1533=FACE_OUTER_BOUND ( 'NONE', #2534, .T. ) ;
#1539=AXIS2_PLACEMENT_3D ( 'NONE', #10294, #6141, #1430 ) ;
#1541=COLOUR_RGB ( '', 0.66274510, 0.83137255, 0.94901961) ;
#1565=( NAMED_UNIT ( * ) SI_UNIT ( $, .STERADIAN. ) SOLID_ANGLE_UNIT ( ) );
#1575=ORIENTED_EDGE ( 'NONE', *, *, #6363, .T. ) ;
#1588=ORIENTED_EDGE ( 'NONE', *, *, #2160, .F. ) ;
#1607=DIRECTION ( 'NONE',  ( 0.000000000000000000, 1.000000000000000000, -1.320393690296331133E-15 ) ) ;
#1617=CIRCLE ( 'NONE', #9576, 1.500000000000000222 ) ;
#1620=ORIENTED_EDGE ( 'NONE', *, *, #8293, .F. ) ;
#1630=ORIENTED_EDGE ( 'NONE', *, *, #9453, .F. ) ;
#1633=ORIENTED_EDGE ( 'NONE', *, *, #8504, .T. ) ;
#1665=LINE ( 'NONE', #6477, #5589 ) ;
#1669=ORIENTED_EDGE ( 'NONE', *, *, #4036, .F. ) ;
#1674=EDGE_LOOP ( 'NONE', ( #7911, #6354, #704, #39, #1693 ) ) ;
#1685=DIRECTION ( 'NONE',  ( 0.000000000000000000, 1.000000000000000000, -1.224646799147353207E-16 ) ) ;
#1693=ORIENTED_EDGE ( 'NONE', *, *, #7532, .T. ) ;
#1694=CLOSED_SHELL ( 'NONE', ( #8951, #7126, #899, #6555, #3591, #5158, #1826, #7597, #6877, #2925, #6151, #9389, #5773, #7219, #4790, #2772, #10485, #7051, #1245, #8375, #10268, #69, #7794, #9093, #94, #4327, #5644 ) ) ;
#1706=AXIS2_PLACEMENT_3D ( 'NONE', #9359, #603, #2095 ) ;
#1725=DIRECTION ( 'NONE',  ( -1.000000000000000000, -0.000000000000000000, -0.000000000000000000 ) ) ;
#1762=AXIS2_PLACEMENT_3D ( 'NONE', #4501, #7745, #326 ) ;
#1826=ADVANCED_FACE ( 'NONE', ( #6972, #7023 ), #6870, .T. ) ;
#1859=AXIS2_PLACEMENT_3D ( 'NONE', #7384, #75, #2411 ) ;
#1868=AXIS2_PLACEMENT_3D ( 'NONE', #5235, #2910, #6230 ) ;
#1901=EDGE_CURVE ( 'NONE', #7181, #798, #2211, .T. ) ;
#1916=EDGE_LOOP ( 'NONE', ( #10342, #10284, #8668 ) ) ;
#1943=EDGE_CURVE ( 'NONE', #65, #8703, #7302, .T. ) ;
#1956=EDGE_CURVE ( 'NONE', #7946, #8610, #7812, .T. ) ;
#1959=CARTESIAN_POINT ( 'NONE',  ( 1.300000000000000044, 1.108512516844082141, 0.6399999999999991251 ) ) ;
#2013=CARTESIAN_POINT ( 'NONE',  ( 1.300000000000000044, 0.7390083445627193548, -1.280000000000000693 ) ) ;
#2023=CARTESIAN_POINT ( 'NONE',  ( -31.74999999999995737, 0.000000000000000000, 0.000000000000000000 ) ) ;
#2033=AXIS2_PLACEMENT_3D ( 'NONE', #10337, #9649, #2376 ) ;
#2038=ORIENTED_EDGE ( 'NONE', *, *, #3451, .T. ) ;
#2064=DIRECTION ( 'NONE',  ( 0.000000000000000000, 0.000000000000000000, 1.000000000000000000 ) ) ;
#2095=DIRECTION ( 'NONE',  ( 0.000000000000000000, 0.4999999999999992228, -0.8660254037844390407 ) ) ;
#2101=AXIS2_PLACEMENT_3D ( 'NONE', #7090, #5610, #4547 ) ;
#2108=DIRECTION ( 'NONE',  ( 0.000000000000000000, -0.5000000000000013323, -0.8660254037844378194 ) ) ;
#2109=VECTOR ( 'NONE', #3652, 1000.000000000000000 ) ;
#2118=DIRECTION ( 'NONE',  ( 0.000000000000000000, -0.5000000000000009992, -0.8660254037844380415 ) ) ;
#2131=CIRCLE ( 'NONE', #5510, 0.1000000000000000472 ) ;
#2143=DIRECTION ( 'NONE',  ( -1.000000000000000000, -0.000000000000000000, -0.000000000000000000 ) ) ;
#2160=EDGE_CURVE ( 'NONE', #2545, #3971, #6104, .T. ) ;
#2163=ORIENTED_EDGE ( 'NONE', *, *, #6363, .F. ) ;
#2171=EDGE_CURVE ( 'NONE', #6915, #2633, #5314, .T. ) ;
#2178=FACE_OUTER_BOUND ( 'NONE', #9038, .T. ) ;
#2211=LINE ( 'NONE', #2797, #1374 ) ;
#2215=VECTOR ( 'NONE', #10151, 1000.000000000000114 ) ;
#2222=VECTOR ( 'NONE', #1288, 1000.000000000000000 ) ;
#2242=ORIENTED_EDGE ( 'NONE', *, *, #721, .T. ) ;
#2250=DIRECTION ( 'NONE',  ( 0.000000000000000000, -0.5000000000000013323, -0.8660254037844378194 ) ) ;
#2268=ORIENTED_EDGE ( 'NONE', *, *, #734, .T. ) ;
#2304=CARTESIAN_POINT ( 'NONE',  ( 0.000000000000000000, 1.478016689125442484, -1.626303258728256651E-15 ) ) ;
#2307=UNCERTAINTY_MEASURE_WITH_UNIT (LENGTH_MEASURE( 1.000000000000000082E-05 ), #2584, 'distance_accuracy_value', 'NONE');
#2314=LINE ( 'NONE', #5537, #1333 ) ;
#2324=ORIENTED_EDGE ( 'NONE', *, *, #1943, .F. ) ;
#2353=DIRECTION ( 'NONE',  ( 0.000000000000000000, 0.000000000000000000, -1.000000000000000000 ) ) ;
#2354=( NAMED_UNIT ( * ) PLANE_ANGLE_UNIT ( ) SI_UNIT ( $, .RADIAN. ) );
#2371=ORIENTED_EDGE ( 'NONE', *, *, #10190, .T. ) ;
#2376=DIRECTION ( 'NONE',  ( 0.000000000000000000, 0.000000000000000000, -1.000000000000000000 ) ) ;
#2411=DIRECTION ( 'NONE',  ( 0.000000000000000000, 0.000000000000000000, -1.000000000000000000 ) ) ;
#2420=VERTEX_POINT ( 'NONE', #3786 ) ;
#2432=LINE ( 'NONE', #4756, #9583 ) ;
#2482=ORIENTED_EDGE ( 'NONE', *, *, #6236, .F. ) ;
#2483=AXIS2_PLACEMENT_3D ( 'NONE', #2023, #284, #1125 ) ;
#2519=CYLINDRICAL_SURFACE ( 'NONE', #7474, 1.500000000000000222 ) ;
#2520=PLANE ( 'NONE',  #6097 ) ;
#2534=EDGE_LOOP ( 'NONE', ( #3784, #7396, #7123 ) ) ;
#2539=EDGE_LOOP ( 'NONE', ( #2163, #8454, #6390, #2826 ) ) ;
#2540=AXIS2_PLACEMENT_3D ( 'NONE', #763, #3997, #2353 ) ;
#2545=VERTEX_POINT ( 'NONE', #557 ) ;
#2568=SURFACE_STYLE_USAGE ( .BOTH. , #9034 ) ;
#2584=( LENGTH_UNIT ( ) NAMED_UNIT ( * ) SI_UNIT ( .MILLI., .METRE. ) );
#2594=ORIENTED_EDGE ( 'NONE', *, *, #5708, .T. ) ;
#2625=DIRECTION ( 'NONE',  ( 0.000000000000000000, 0.000000000000000000, 1.000000000000000000 ) ) ;
#2633=VERTEX_POINT ( 'NONE', #1403 ) ;
#2636=VERTEX_POINT ( 'NONE', #8833 ) ;
#2682=EDGE_CURVE ( 'NONE', #3139, #3971, #362, .T. ) ;
#2712=DIRECTION ( 'NONE',  ( -0.000000000000000000, 0.8660254037844391517, 0.4999999999999991118 ) ) ;
#2731=AXIS2_PLACEMENT_3D ( 'NONE', #725, #5540, #10443 ) ;
#2772=ADVANCED_FACE ( 'NONE', ( #4255 ), #9847, .F. ) ;
#2787=ORIENTED_EDGE ( 'NONE', *, *, #3451, .F. ) ;
#2794=STYLED_ITEM ( 'NONE', ( #8362 ), #9161 ) ;
#2797=CARTESIAN_POINT ( 'NONE',  ( 1.300000000000000044, 1.478016689125442484, -1.626303258728256651E-15 ) ) ;
#2802=FACE_OUTER_BOUND ( 'NONE', #9843, .T. ) ;
#2826=ORIENTED_EDGE ( 'NONE', *, *, #2998, .F. ) ;
#2855=DIRECTION ( 'NONE',  ( 1.000000000000000000, 0.000000000000000000, 0.000000000000000000 ) ) ;
#2860=EDGE_CURVE ( 'NONE', #8371, #6113, #4584, .T. ) ;
#2864=CARTESIAN_POINT ( 'NONE',  ( 0.1499999999999973577, 0.000000000000000000, 0.000000000000000000 ) ) ;
#2910=DIRECTION ( 'NONE',  ( -1.000000000000000000, -0.000000000000000000, -0.000000000000000000 ) ) ;
#2911=VERTEX_POINT ( 'NONE', #4899 ) ;
#2912=PLANE ( 'NONE',  #4381 ) ;
#2914=CARTESIAN_POINT ( 'NONE',  ( 1.300000000000000044, -0.7390083445627200209, 1.280000000000001137 ) ) ;
#2925=ADVANCED_FACE ( 'NONE', ( #136 ), #2519, .T. ) ;
#2932=CIRCLE ( 'NONE', #5633, 2.750000000000000000 ) ;
#2934=EDGE_CURVE ( 'NONE', #6822, #5643, #6618, .T. ) ;
#2959=DIRECTION ( 'NONE',  ( 1.000000000000000000, 0.000000000000000000, 0.000000000000000000 ) ) ;
#2989=DIRECTION ( 'NONE',  ( 0.000000000000000000, -0.4999999999999992784, 0.8660254037844390407 ) ) ;
#2992=ORIENTED_EDGE ( 'NONE', *, *, #2934, .T. ) ;
#2998=EDGE_CURVE ( 'NONE', #5643, #6822, #3740, .T. ) ;
#3005=DIRECTION ( 'NONE',  ( -1.000000000000000000, -0.000000000000000000, -0.000000000000000000 ) ) ;
#3021=DIRECTION ( 'NONE',  ( 0.000000000000000000, 0.8660254037844380415, -0.5000000000000009992 ) ) ;
#3024=CARTESIAN_POINT ( 'NONE',  ( 1.300000000000000044, 1.478016689125442484, -1.626303258728256651E-15 ) ) ;
#3066=AXIS2_PLACEMENT_3D ( 'NONE', #8718, #7287, #9471 ) ;
#3107=CARTESIAN_POINT ( 'NONE',  ( 3.099999999999998757, 0.000000000000000000, 0.000000000000000000 ) ) ;
#3108=EDGE_LOOP ( 'NONE', ( #743, #8169, #2482 ) ) ;
#3115=LINE ( 'NONE', #8788, #675 ) ;
#3139=VERTEX_POINT ( 'NONE', #10259 ) ;
#3142=CARTESIAN_POINT ( 'NONE',  ( 3.000000000000000888, 2.750000000000000000, 0.000000000000000000 ) ) ;
#3164=ORIENTED_EDGE ( 'NONE', *, *, #9984, .F. ) ;
#3171=DIRECTION ( 'NONE',  ( 1.000000000000000000, 0.000000000000000000, 0.000000000000000000 ) ) ;
#3194=FACE_OUTER_BOUND ( 'NONE', #8679, .T. ) ;
#3200=FACE_OUTER_BOUND ( 'NONE', #6548, .T. ) ;
#3212=ORIENTED_EDGE ( 'NONE', *, *, #2860, .F. ) ;
#3222=DIRECTION ( 'NONE',  ( -1.000000000000000000, -0.000000000000000000, -0.000000000000000000 ) ) ;
#3230=ORIENTED_EDGE ( 'NONE', *, *, #3307, .T. ) ;
#3239=DIRECTION ( 'NONE',  ( 0.000000000000000000, 0.000000000000000000, 1.000000000000000000 ) ) ;
#3274=VECTOR ( 'NONE', #756, 1000.000000000000000 ) ;
#3283=AXIS2_PLACEMENT_3D ( 'NONE', #9724, #6630, #9882 ) ;
#3298=CARTESIAN_POINT ( 'NONE',  ( 0.000000000000000000, -1.478016689125442706, 1.843143693225357538E-15 ) ) ;
#3307=EDGE_CURVE ( 'NONE', #165, #2420, #9414, .T. ) ;
#3351=CARTESIAN_POINT ( 'NONE',  ( 1.300000000000000044, 0.000000000000000000, 0.000000000000000000 ) ) ;
#3357=CARTESIAN_POINT ( 'NONE',  ( 1.300000000000000044, 1.478016689125442484, -1.626303258728256651E-15 ) ) ;
#3413=DIRECTION ( 'NONE',  ( -1.000000000000000000, -0.000000000000000000, -0.000000000000000000 ) ) ;
#3418=DIRECTION ( 'NONE',  ( 0.000000000000000000, -1.000000000000000000, 1.320393690296331133E-15 ) ) ;
#3451=EDGE_CURVE ( 'NONE', #65, #165, #176, .T. ) ;
#3458=CARTESIAN_POINT ( 'NONE',  ( -31.74999999999995737, 3.367778697655221012E-16, -2.750000000000000000 ) ) ;
#3468=DIRECTION ( 'NONE',  ( -0.000000000000000000, 1.320393690296331133E-15, 1.000000000000000000 ) ) ;
#3469=DIRECTION ( 'NONE',  ( 0.000000000000000000, 0.8660254037844379305, -0.5000000000000014433 ) ) ;
#3488=ORIENTED_EDGE ( 'NONE', *, *, #10079, .F. ) ;
#3547=EDGE_CURVE ( 'NONE', #6004, #6822, #2131, .T. ) ;
#3566=( GEOMETRIC_REPRESENTATION_CONTEXT ( 3 ) GLOBAL_UNCERTAINTY_ASSIGNED_CONTEXT ( ( #1455 ) ) GLOBAL_UNIT_ASSIGNED_CONTEXT ( ( #7334, #2354, #1565 ) ) REPRESENTATION_CONTEXT ( 'NONE', 'WORKASPACE' ) );
#3591=ADVANCED_FACE ( 'NONE', ( #8344 ), #1073, .T. ) ;
#3595=CARTESIAN_POINT ( 'NONE',  ( -31.74999999999995737, 0.000000000000000000, 0.000000000000000000 ) ) ;
#3603=DIRECTION ( 'NONE',  ( 1.000000000000000000, 0.000000000000000000, 0.000000000000000000 ) ) ;
#3608=DIRECTION ( 'NONE',  ( 0.000000000000000000, 0.000000000000000000, 1.000000000000000000 ) ) ;
#3616=EDGE_LOOP ( 'NONE', ( #404, #1630, #6718, #4803 ) ) ;
#3628=( NAMED_UNIT ( * ) SI_UNIT ( $, .STERADIAN. ) SOLID_ANGLE_UNIT ( ) );
#3649=EDGE_CURVE ( 'NONE', #2420, #8610, #4666, .T. ) ;
#3652=DIRECTION ( 'NONE',  ( 0.000000000000000000, -1.000000000000000000, 1.026972870230479989E-15 ) ) ;
#3655=ORIENTED_EDGE ( 'NONE', *, *, #2171, .F. ) ;
#3693=VERTEX_POINT ( 'NONE', #6245 ) ;
#3700=EDGE_LOOP ( 'NONE', ( #5410, #5213 ) ) ;
#3726=AXIS2_PLACEMENT_3D ( 'NONE', #10017, #7614, #358 ) ;
#3734=EDGE_CURVE ( 'NONE', #2636, #10382, #3815, .T. ) ;
#3740=CIRCLE ( 'NONE', #9692, 1.600000000000000311 ) ;
#3756=CARTESIAN_POINT ( 'NONE',  ( 11.00000000000000355, 1.493456771560197319E-16, -1.219500000000000028 ) ) ;
#3775=CARTESIAN_POINT ( 'NONE',  ( 3.000000000000002665, 0.000000000000000000, 2.750000000000000000 ) ) ;
#3784=ORIENTED_EDGE ( 'NONE', *, *, #8564, .T. ) ;
#3786=CARTESIAN_POINT ( 'NONE',  ( 0.1499999999999973577, 0.000000000000000000, 2.750000000000000000 ) ) ;
#3795=ORIENTED_EDGE ( 'NONE', *, *, #2160, .T. ) ;
#3813=FACE_OUTER_BOUND ( 'NONE', #7936, .T. ) ;
#3815=LINE ( 'NONE', #9505, #7555 ) ;
#3842=EDGE_LOOP ( 'NONE', ( #6117, #4524, #5236, #1588 ) ) ;
#3869=AXIS2_PLACEMENT_3D ( 'NONE', #5511, #7372, #5664 ) ;
#3871=EDGE_CURVE ( 'NONE', #520, #5053, #5819, .T. ) ;
#3873=LINE ( 'NONE', #9565, #3274 ) ;
#3892=ORIENTED_EDGE ( 'NONE', *, *, #6801, .T. ) ;
#3958=EDGE_LOOP ( 'NONE', ( #4819, #1620, #3212 ) ) ;
#3959=AXIS2_PLACEMENT_3D ( 'NONE', #6192, #3021, #10348 ) ;
#3970=CIRCLE ( 'NONE', #9027, 2.750000000000000000 ) ;
#3971=VERTEX_POINT ( 'NONE', #6 ) ;
#3993=LINE ( 'NONE', #3298, #9934 ) ;
#3997=DIRECTION ( 'NONE',  ( 1.000000000000000000, 0.000000000000000000, 0.000000000000000000 ) ) ;
#3999=PRESENTATION_STYLE_ASSIGNMENT (( #2568 ) ) ;
#4026=ORIENTED_EDGE ( 'NONE', *, *, #4757, .F. ) ;
#4036=EDGE_CURVE ( 'NONE', #8297, #2636, #162, .T. ) ;
#4044=PLANE ( 'NONE',  #2540 ) ;
#4077=CIRCLE ( 'NONE', #357, 1.280000000000000027 ) ;
#4090=AXIS2_PLACEMENT_3D ( 'NONE', #5888, #8987, #2625 ) ;
#4101=CARTESIAN_POINT ( 'NONE',  ( 1.300000000000000044, 0.7390083445627193548, -1.280000000000000693 ) ) ;
#4105=VERTEX_POINT ( 'NONE', #5919 ) ;
#4112=ORIENTED_EDGE ( 'NONE', *, *, #9268, .T. ) ;
#4123=ORIENTED_EDGE ( 'NONE', *, *, #10148, .T. ) ;
#4139=DIRECTION ( 'NONE',  ( 1.000000000000000000, 0.000000000000000000, 0.000000000000000000 ) ) ;
#4157=DIRECTION ( 'NONE',  ( 0.000000000000000000, 0.000000000000000000, 1.000000000000000000 ) ) ;
#4172=VERTEX_POINT ( 'NONE', #9925 ) ;
#4179=APPLICATION_CONTEXT ( 'automotive_design' ) ;
#4255=FACE_OUTER_BOUND ( 'NONE', #1674, .T. ) ;
#4264=SURFACE_SIDE_STYLE ('',( #10113 ) ) ;
#4274=ORIENTED_EDGE ( 'NONE', *, *, #5334, .T. ) ;
#4327=ADVANCED_FACE ( 'NONE', ( #1533 ), #2912, .F. ) ;
#4366=EDGE_LOOP ( 'NONE', ( #4858, #5604, #2371, #3892, #9620, #4026 ) ) ;
#4381=AXIS2_PLACEMENT_3D ( 'NONE', #6130, #4646, #9382 ) ;
#4382=FACE_OUTER_BOUND ( 'NONE', #5666, .T. ) ;
#4431=CARTESIAN_POINT ( 'NONE',  ( 3.000000000000002665, 0.000000000000000000, 0.000000000000000000 ) ) ;
#4455=EDGE_CURVE ( 'NONE', #2545, #8537, #9138, .T. ) ;
#4501=CARTESIAN_POINT ( 'NONE',  ( 1.300000000000000044, 1.478016689125442484, -1.626303258728256651E-15 ) ) ;
#4513=CARTESIAN_POINT ( 'NONE',  ( 0.000000000000000000, 1.478016689125442484, -1.626303258728256651E-15 ) ) ;
#4516=CARTESIAN_POINT ( 'NONE',  ( 11.00000000000000355, 1.665213485140613626E-16, -1.219500000000000028 ) ) ;
#4524=ORIENTED_EDGE ( 'NONE', *, *, #9504, .T. ) ;
#4539=EDGE_LOOP ( 'NONE', ( #7448, #1669, #888, #6649, #6810 ) ) ;
#4547=DIRECTION ( 'NONE',  ( 1.000000000000000000, 0.000000000000000000, 0.000000000000000000 ) ) ;
#4567=PRODUCT_DEFINITION ( 'UNKNOWN', '', #6508, #9375 ) ;
#4573=AXIS2_PLACEMENT_3D ( 'NONE', #4101, #8979, #4947 ) ;
#4580=AXIS2_PLACEMENT_3D ( 'NONE', #6224, #9318, #1208 ) ;
#4584=CIRCLE ( 'NONE', #4090, 1.280000000000000027 ) ;
#4617=CARTESIAN_POINT ( 'NONE',  ( 1.300000000000000044, -1.108512516844082141, -0.6399999999999991251 ) ) ;
#4622=VECTOR ( 'NONE', #15, 1000.000000000000000 ) ;
#4633=CARTESIAN_POINT ( 'NONE',  ( 1.300000000000000044, 1.108512516844080364, -0.6400000000000017897 ) ) ;
#4641=ORIENTED_EDGE ( 'NONE', *, *, #3871, .T. ) ;
#4646=DIRECTION ( 'NONE',  ( 1.000000000000000000, 0.000000000000000000, 0.000000000000000000 ) ) ;
#4660=CARTESIAN_POINT ( 'NONE',  ( 1.300000000000000044, 0.000000000000000000, 0.000000000000000000 ) ) ;
#4666=CIRCLE ( 'NONE', #9423, 0.1499999999999999667 ) ;
#4742=CARTESIAN_POINT ( 'NONE',  ( 1.300000000000000044, 0.7390083445627193548, -1.280000000000000693 ) ) ;
#4748=DIRECTION ( 'NONE',  ( 0.000000000000000000, 0.000000000000000000, 1.000000000000000000 ) ) ;
#4756=CARTESIAN_POINT ( 'NONE',  ( 1.300000000000000044, 0.7390083445627224634, 1.279999999999999138 ) ) ;
#4757=EDGE_CURVE ( 'NONE', #6915, #2636, #9465, .T. ) ;
#4764=EDGE_LOOP ( 'NONE', ( #10009, #2594, #418, #5791, #6261 ) ) ;
#4790=ADVANCED_FACE ( 'NONE', ( #8664 ), #9524, .T. ) ;
#4803=ORIENTED_EDGE ( 'NONE', *, *, #1956, .F. ) ;
#4819=ORIENTED_EDGE ( 'NONE', *, *, #9980, .T. ) ;
#4858=ORIENTED_EDGE ( 'NONE', *, *, #2171, .T. ) ;
#4870=ORIENTED_EDGE ( 'NONE', *, *, #3547, .F. ) ;
#4876=DIRECTION ( 'NONE',  ( 0.000000000000000000, -0.4999999999999992784, 0.8660254037844390407 ) ) ;
#4885=DIRECTION ( 'NONE',  ( -1.000000000000000000, -0.000000000000000000, -0.000000000000000000 ) ) ;
#4899=CARTESIAN_POINT ( 'NONE',  ( 0.000000000000000000, -0.7390083445627200209, 1.280000000000001137 ) ) ;
#4908=EDGE_CURVE ( 'NONE', #3971, #4105, #1665, .T. ) ;
#4914=CARTESIAN_POINT ( 'NONE',  ( 0.000000000000000000, 3.275930187719169848E-16, -2.600000000000000089 ) ) ;
#4920=VECTOR ( 'NONE', #495, 1000.000000000000227 ) ;
#4926=ORIENTED_EDGE ( 'NONE', *, *, #8093, .T. ) ;
#4939=CARTESIAN_POINT ( 'NONE',  ( 3.099999999999998757, 0.000000000000000000, 0.000000000000000000 ) ) ;
#4947=DIRECTION ( 'NONE',  ( 0.000000000000000000, 1.000000000000000000, -1.026972870230479989E-15 ) ) ;
#5033=CARTESIAN_POINT ( 'NONE',  ( 1.300000000000000044, 0.7390083445627193548, -1.280000000000000693 ) ) ;
#5045=DIRECTION ( 'NONE',  ( 0.000000000000000000, 0.4999999999999991673, -0.8660254037844391517 ) ) ;
#5053=VERTEX_POINT ( 'NONE', #7095 ) ;
#5079=LINE ( 'NONE', #5917, #5403 ) ;
#5146=DIRECTION ( 'NONE',  ( 0.000000000000000000, -1.000000000000000000, 0.000000000000000000 ) ) ;
#5157=CARTESIAN_POINT ( 'NONE',  ( 1.300000000000000044, -0.7390083445627200209, 1.280000000000001137 ) ) ;
#5158=ADVANCED_FACE ( 'NONE', ( #3813 ), #583, .T. ) ;
#5160=CONICAL_SURFACE ( 'NONE', #7371, 1.219500000000000028, 0.7853981633974680410 ) ;
#5184=EDGE_LOOP ( 'NONE', ( #3655, #5953, #2268, #10023, #84 ) ) ;
#5197=CARTESIAN_POINT ( 'NONE',  ( 3.099999999999998757, 0.000000000000000000, -1.600000000000000311 ) ) ;
#5208=VERTEX_POINT ( 'NONE', #4617 ) ;
#5213=ORIENTED_EDGE ( 'NONE', *, *, #595, .F. ) ;
#5235=CARTESIAN_POINT ( 'NONE',  ( 1.300000000000000044, 0.000000000000000000, 0.000000000000000000 ) ) ;
#5236=ORIENTED_EDGE ( 'NONE', *, *, #721, .F. ) ;
#5246=DIRECTION ( 'NONE',  ( 0.000000000000000000, 0.000000000000000000, 1.000000000000000000 ) ) ;
#5255=CARTESIAN_POINT ( 'NONE',  ( 1.300000000000000044, -1.478016689125442706, 1.843143693225357538E-15 ) ) ;
#5314=LINE ( 'NONE', #4513, #8490 ) ;
#5334=EDGE_CURVE ( 'NONE', #520, #5208, #6953, .T. ) ;
#5335=AXIS2_PLACEMENT_3D ( 'NONE', #7029, #1472, #8000 ) ;
#5340=ORIENTED_EDGE ( 'NONE', *, *, #4036, .T. ) ;
#5403=VECTOR ( 'NONE', #9173, 1000.000000000000000 ) ;
#5410=ORIENTED_EDGE ( 'NONE', *, *, #4455, .F. ) ;
#5417=EDGE_LOOP ( 'NONE', ( #8906, #10018, #1442, #6902, #9457 ) ) ;
#5445=LINE ( 'NONE', #2013, #2109 ) ;
#5456=FACE_OUTER_BOUND ( 'NONE', #3616, .T. ) ;
#5467=DIRECTION ( 'NONE',  ( -1.000000000000000000, -0.000000000000000000, -0.000000000000000000 ) ) ;
#5506=AXIS2_PLACEMENT_3D ( 'NONE', #2864, #6088, #3608 ) ;
#5510=AXIS2_PLACEMENT_3D ( 'NONE', #5197, #5146, #9185 ) ;
#5511=CARTESIAN_POINT ( 'NONE',  ( 10.71950000000001424, 0.000000000000000000, 0.000000000000000000 ) ) ;
#5537=CARTESIAN_POINT ( 'NONE',  ( -31.74999999999995737, 0.000000000000000000, 2.750000000000000000 ) ) ;
#5540=DIRECTION ( 'NONE',  ( -1.000000000000000000, -0.000000000000000000, -0.000000000000000000 ) ) ;
#5560=DIRECTION ( 'NONE',  ( 0.000000000000000000, -1.000000000000000000, 1.026972870230479989E-15 ) ) ;
#5563=AXIS2_PLACEMENT_3D ( 'NONE', #3107, #2855, #6077 ) ;
#5576=DIRECTION ( 'NONE',  ( 0.000000000000000000, 0.000000000000000000, 1.000000000000000000 ) ) ;
#5589=VECTOR ( 'NONE', #29, 1000.000000000000000 ) ;
#5604=ORIENTED_EDGE ( 'NONE', *, *, #7737, .F. ) ;
#5610=DIRECTION ( 'NONE',  ( 0.000000000000000000, 0.000000000000000000, 1.000000000000000000 ) ) ;
#5633=AXIS2_PLACEMENT_3D ( 'NONE', #9124, #3603, #5246 ) ;
#5643=VERTEX_POINT ( 'NONE', #6936 ) ;
#5644=ADVANCED_FACE ( 'NONE', ( #9607 ), #9918, .F. ) ;
#5661=DIRECTION ( 'NONE',  ( 0.000000000000000000, 0.000000000000000000, -1.000000000000000000 ) ) ;
#5663=CARTESIAN_POINT ( 'NONE',  ( 1.300000000000000044, -1.478016689125442706, 1.843143693225357538E-15 ) ) ;
#5664=DIRECTION ( 'NONE',  ( 0.000000000000000000, 0.000000000000000000, 1.000000000000000000 ) ) ;
#5666=EDGE_LOOP ( 'NONE', ( #2787, #9076, #8420, #7825 ) ) ;
#5675=CARTESIAN_POINT ( 'NONE',  ( 3.000000000000000000, 0.000000000000000000, -1.600000000000000311 ) ) ;
#5688=FACE_OUTER_BOUND ( 'NONE', #4539, .T. ) ;
#5708=EDGE_CURVE ( 'NONE', #729, #4172, #8067, .T. ) ;
#5718=CARTESIAN_POINT ( 'NONE',  ( 0.000000000000000000, -0.7390083445627200209, 1.280000000000001137 ) ) ;
#5773=ADVANCED_FACE ( 'NONE', ( #8012 ), #9228, .F. ) ;
#5788=EDGE_LOOP ( 'NONE', ( #3164, #8880, #9916, #8089 ) ) ;
#5791=ORIENTED_EDGE ( 'NONE', *, *, #7611, .T. ) ;
#5793=AXIS2_PLACEMENT_3D ( 'NONE', #840, #3171, #8369 ) ;
#5819=LINE ( 'NONE', #5663, #7388 ) ;
#5835=LINE ( 'NONE', #6790, #697 ) ;
#5843=CARTESIAN_POINT ( 'NONE',  ( 1.300000000000000044, 1.690103923579304181E-15, 1.280000000000000249 ) ) ;
#5888=CARTESIAN_POINT ( 'NONE',  ( 1.300000000000000044, 0.000000000000000000, 0.000000000000000000 ) ) ;
#5893=CIRCLE ( 'NONE', #835, 1.219500000000000028 ) ;
#5917=CARTESIAN_POINT ( 'NONE',  ( 1.300000000000000044, -0.7390083445627200209, 1.280000000000001137 ) ) ;
#5919=CARTESIAN_POINT ( 'NONE',  ( 3.099999999999998757, 0.000000000000000000, 1.500000000000000222 ) ) ;
#5931=DIRECTION ( 'NONE',  ( 0.000000000000000000, -0.4999999999999991118, 0.8660254037844391517 ) ) ;
#5934=CARTESIAN_POINT ( 'NONE',  ( 0.1499999999999973577, 3.367778697655221012E-16, -2.750000000000000000 ) ) ;
#5941=DIRECTION ( 'NONE',  ( 0.000000000000000000, 0.000000000000000000, -1.000000000000000000 ) ) ;
#5953=ORIENTED_EDGE ( 'NONE', *, *, #9762, .F. ) ;
#5961=VECTOR ( 'NONE', #1607, 1000.000000000000000 ) ;
#5966=ORIENTED_EDGE ( 'NONE', *, *, #2682, .F. ) ;
#5970=VECTOR ( 'NONE', #8286, 1000.000000000000114 ) ;
#5992=CARTESIAN_POINT ( 'NONE',  ( 0.000000000000000000, 0.000000000000000000, 2.600000000000000089 ) ) ;
#6004=VERTEX_POINT ( 'NONE', #368 ) ;
#6007=CARTESIAN_POINT ( 'NONE',  ( 0.1499999999999973577, 3.184081677783118191E-16, -2.600000000000000089 ) ) ;
#6029=EDGE_CURVE ( 'NONE', #4105, #6004, #1617, .T. ) ;
#6051=FILL_AREA_STYLE_COLOUR ( '', #7540 ) ;
#6052=ORIENTED_EDGE ( 'NONE', *, *, #2934, .F. ) ;
#6070=CARTESIAN_POINT ( 'NONE',  ( 11.00000000000000355, 0.000000000000000000, 0.000000000000000000 ) ) ;
#6072=DIRECTION ( 'NONE',  ( 0.000000000000000000, 0.000000000000000000, 1.000000000000000000 ) ) ;
#6077=DIRECTION ( 'NONE',  ( 0.000000000000000000, 0.000000000000000000, -1.000000000000000000 ) ) ;
#6088=DIRECTION ( 'NONE',  ( -1.000000000000000000, -0.000000000000000000, -0.000000000000000000 ) ) ;
#6097=AXIS2_PLACEMENT_3D ( 'NONE', #7447, #3469, #6694 ) ;
#6104=LINE ( 'NONE', #9407, #2222 ) ;
#6113=VERTEX_POINT ( 'NONE', #1959 ) ;
#6117=ORIENTED_EDGE ( 'NONE', *, *, #4455, .T. ) ;
#6130=CARTESIAN_POINT ( 'NONE',  ( 1.300000000000000044, 1.478016689125442484, -1.626303258728256651E-15 ) ) ;
#6136=AXIS2_PLACEMENT_3D ( 'NONE', #9332, #627, #474 ) ;
#6141=DIRECTION ( 'NONE',  ( -1.000000000000000000, -0.000000000000000000, -0.000000000000000000 ) ) ;
#6151=ADVANCED_FACE ( 'NONE', ( #2802 ), #5160, .T. ) ;
#6185=AXIS2_PLACEMENT_3D ( 'NONE', #7584, #2712, #5931 ) ;
#6192=CARTESIAN_POINT ( 'NONE',  ( 1.300000000000000044, -0.7390083445627200209, 1.280000000000001137 ) ) ;
#6196=EDGE_CURVE ( 'NONE', #4172, #8945, #7834, .T. ) ;
#6223=EDGE_CURVE ( 'NONE', #3693, #2633, #2432, .T. ) ;
#6224=CARTESIAN_POINT ( 'NONE',  ( 0.000000000000000000, 0.000000000000000000, 0.000000000000000000 ) ) ;
#6230=DIRECTION ( 'NONE',  ( 0.000000000000000000, 0.000000000000000000, 1.000000000000000000 ) ) ;
#6236=EDGE_CURVE ( 'NONE', #6113, #798, #592, .T. ) ;
#6245=CARTESIAN_POINT ( 'NONE',  ( 1.300000000000000044, 0.7390083445627224634, 1.279999999999999138 ) ) ;
#6261=ORIENTED_EDGE ( 'NONE', *, *, #10079, .T. ) ;
#6337=AXIS2_PLACEMENT_3D ( 'NONE', #7208, #8854, #5661 ) ;
#6348=CIRCLE ( 'NONE', #8560, 0.1000000000000000472 ) ;
#6354=ORIENTED_EDGE ( 'NONE', *, *, #6223, .F. ) ;
#6360=CARTESIAN_POINT ( 'NONE',  ( 1.300000000000000044, 0.000000000000000000, 1.280000000000000027 ) ) ;
#6363=EDGE_CURVE ( 'NONE', #4105, #5643, #6348, .T. ) ;
#6369=DIRECTION ( 'NONE',  ( 0.000000000000000000, 0.000000000000000000, -1.000000000000000000 ) ) ;
#6386=ORIENTED_EDGE ( 'NONE', *, *, #9268, .F. ) ;
#6390=ORIENTED_EDGE ( 'NONE', *, *, #3547, .T. ) ;
#6396=CARTESIAN_POINT ( 'NONE',  ( 3.000000000000002665, 0.000000000000000000, 0.000000000000000000 ) ) ;
#6400=ORIENTED_EDGE ( 'NONE', *, *, #9146, .T. ) ;
#6406=CARTESIAN_POINT ( 'NONE',  ( 1.300000000000000044, 1.478016689125442484, -1.626303258728256651E-15 ) ) ;
#6425=AXIS2_PLACEMENT_3D ( 'NONE', #3595, #6821, #6072 ) ;
#6444=ORIENTED_EDGE ( 'NONE', *, *, #6196, .F. ) ;
#6467=LINE ( 'NONE', #5718, #5970 ) ;
#6477=CARTESIAN_POINT ( 'NONE',  ( -31.74999999999995737, 0.000000000000000000, 1.500000000000000222 ) ) ;
#6486=AXIS2_PLACEMENT_3D ( 'NONE', #4939, #4139, #6676 ) ;
#6508=PRODUCT_DEFINITION_FORMATION_WITH_SPECIFIED_SOURCE ( 'ANY', '', #56, .NOT_KNOWN. ) ;
#6531=TOROIDAL_SURFACE ( 'NONE', #1458, 2.600000000000000089, 0.1499999999999999944 ) ;
#6548=EDGE_LOOP ( 'NONE', ( #9227, #667, #6444, #7685, #5340 ) ) ;
#6555=ADVANCED_FACE ( 'NONE', ( #8465 ), #9754, .T. ) ;
#6577=VECTOR ( 'NONE', #4876, 1000.000000000000000 ) ;
#6578=DIRECTION ( 'NONE',  ( 0.000000000000000000, 0.000000000000000000, 1.000000000000000000 ) ) ;
#6618=CIRCLE ( 'NONE', #8831, 1.600000000000000311 ) ;
#6630=DIRECTION ( 'NONE',  ( -1.000000000000000000, -0.000000000000000000, -0.000000000000000000 ) ) ;
#6636=FILL_AREA_STYLE ('',( #920 ) ) ;
#6649=ORIENTED_EDGE ( 'NONE', *, *, #1901, .F. ) ;
#6676=DIRECTION ( 'NONE',  ( 0.000000000000000000, 0.000000000000000000, -1.000000000000000000 ) ) ;
#6681=MECHANICAL_DESIGN_GEOMETRIC_PRESENTATION_REPRESENTATION('',(#2794),#9751);
#6694=DIRECTION ( 'NONE',  ( 0.000000000000000000, 0.5000000000000013323, 0.8660254037844378194 ) ) ;
#6702=SURFACE_STYLE_USAGE ( .BOTH. , #4264 ) ;
#6704=DIRECTION ( 'NONE',  ( 0.000000000000000000, 1.224646799147353207E-16, 1.000000000000000000 ) ) ;
#6718=ORIENTED_EDGE ( 'NONE', *, *, #3649, .T. ) ;
#6724=FACE_OUTER_BOUND ( 'NONE', #7833, .T. ) ;
#6790=CARTESIAN_POINT ( 'NONE',  ( 1.300000000000000044, -1.478016689125442706, 1.843143693225357538E-15 ) ) ;
#6801=EDGE_CURVE ( 'NONE', #5053, #10382, #3993, .T. ) ;
#6810=ORIENTED_EDGE ( 'NONE', *, *, #9762, .T. ) ;
#6821=DIRECTION ( 'NONE',  ( -1.000000000000000000, -0.000000000000000000, -0.000000000000000000 ) ) ;
#6822=VERTEX_POINT ( 'NONE', #5675 ) ;
#6836=CARTESIAN_POINT ( 'NONE',  ( 0.1499999999999973577, 0.000000000000000000, 2.600000000000000089 ) ) ;
#6864=DIRECTION ( 'NONE',  ( 0.000000000000000000, -1.224646799147353207E-16, 1.000000000000000000 ) ) ;
#6870=PLANE ( 'NONE',  #4580 ) ;
#6877=ADVANCED_FACE ( 'NONE', ( #7163, #3194 ), #10420, .T. ) ;
#6902=ORIENTED_EDGE ( 'NONE', *, *, #6236, .T. ) ;
#6915=VERTEX_POINT ( 'NONE', #8870 ) ;
#6917=UNCERTAINTY_MEASURE_WITH_UNIT (LENGTH_MEASURE( 1.000000000000000082E-05 ), #251, 'distance_accuracy_value', 'NONE');
#6926=LINE ( 'NONE', #2914, #9367 ) ;
#6936=CARTESIAN_POINT ( 'NONE',  ( 3.000000000000000000, 1.959434878635765477E-16, 1.600000000000000311 ) ) ;
#6953=LINE ( 'NONE', #444, #2215 ) ;
#6972=FACE_BOUND ( 'NONE', #4366, .T. ) ;
#7014=EDGE_CURVE ( 'NONE', #8945, #10382, #8343, .T. ) ;
#7023=FACE_OUTER_BOUND ( 'NONE', #9056, .T. ) ;
#7029=CARTESIAN_POINT ( 'NONE',  ( 1.300000000000000044, 0.000000000000000000, 0.000000000000000000 ) ) ;
#7033=AXIS2_PLACEMENT_3D ( 'NONE', #3142, #811, #6369 ) ;
#7051=ADVANCED_FACE ( 'NONE', ( #6724 ), #9986, .T. ) ;
#7079=ORIENTED_EDGE ( 'NONE', *, *, #10108, .T. ) ;
#7090=CARTESIAN_POINT ( 'NONE',  ( 0.000000000000000000, 0.000000000000000000, 0.000000000000000000 ) ) ;
#7095=CARTESIAN_POINT ( 'NONE',  ( 0.000000000000000000, -1.478016689125442706, 1.843143693225357538E-15 ) ) ;
#7096=DIRECTION ( 'NONE',  ( 0.000000000000000000, 0.000000000000000000, 1.000000000000000000 ) ) ;
#7111=DIRECTION ( 'NONE',  ( 0.000000000000000000, 0.000000000000000000, 1.000000000000000000 ) ) ;
#7123=ORIENTED_EDGE ( 'NONE', *, *, #1260, .F. ) ;
#7126=ADVANCED_FACE ( 'NONE', ( #2178 ), #8729, .T. ) ;
#7153=VECTOR ( 'NONE', #9498, 1000.000000000000000 ) ;
#7163=FACE_BOUND ( 'NONE', #500, .T. ) ;
#7181=VERTEX_POINT ( 'NONE', #3024 ) ;
#7197=FACE_OUTER_BOUND ( 'NONE', #3700, .T. ) ;
#7199=ORIENTED_EDGE ( 'NONE', *, *, #7611, .F. ) ;
#7207=SHAPE_REPRESENTATION ( 'socket head cap screw_iso_ISO 4762 M3 x 8 - 8N', ( #2101 ), #1104 ) ;
#7208=CARTESIAN_POINT ( 'NONE',  ( 3.099999999999998757, 0.000000000000000000, 0.000000000000000000 ) ) ;
#7211=DIRECTION ( 'NONE',  ( -1.000000000000000000, -0.000000000000000000, -0.000000000000000000 ) ) ;
#7219=ADVANCED_FACE ( 'NONE', ( #5456 ), #6531, .T. ) ;
#7233=ORIENTED_EDGE ( 'NONE', *, *, #2998, .T. ) ;
#7246=FACE_OUTER_BOUND ( 'NONE', #1008, .T. ) ;
#7287=DIRECTION ( 'NONE',  ( -1.000000000000000000, -0.000000000000000000, -0.000000000000000000 ) ) ;
#7299=ORIENTED_EDGE ( 'NONE', *, *, #9504, .F. ) ;
#7302=CIRCLE ( 'NONE', #8655, 2.750000000000000000 ) ;
#7318=CARTESIAN_POINT ( 'NONE',  ( 0.1499999999999973577, 0.000000000000000000, 0.000000000000000000 ) ) ;
#7334=( LENGTH_UNIT ( ) NAMED_UNIT ( * ) SI_UNIT ( .MILLI., .METRE. ) );
#7365=AXIS2_PLACEMENT_3D ( 'NONE', #633, #8801, #7902 ) ;
#7371=AXIS2_PLACEMENT_3D ( 'NONE', #6070, #9325, #2064 ) ;
#7372=DIRECTION ( 'NONE',  ( -1.000000000000000000, -0.000000000000000000, -0.000000000000000000 ) ) ;
#7377=LINE ( 'NONE', #121, #4622 ) ;
#7384=CARTESIAN_POINT ( 'NONE',  ( 1.300000000000000044, 1.478016689125442484, -1.626303258728256651E-15 ) ) ;
#7388=VECTOR ( 'NONE', #8959, 1000.000000000000000 ) ;
#7394=DIRECTION ( 'NONE',  ( -1.000000000000000000, -0.000000000000000000, -0.000000000000000000 ) ) ;
#7396=ORIENTED_EDGE ( 'NONE', *, *, #9134, .T. ) ;
#7447=CARTESIAN_POINT ( 'NONE',  ( 1.300000000000000044, 1.478016689125442484, -1.626303258728256651E-15 ) ) ;
#7448=ORIENTED_EDGE ( 'NONE', *, *, #4757, .T. ) ;
#7462=MECHANICAL_DESIGN_GEOMETRIC_PRESENTATION_REPRESENTATION('',(#8647),#3566);
#7470=VECTOR ( 'NONE', #7655, 1000.000000000000114 ) ;
#7474=AXIS2_PLACEMENT_3D ( 'NONE', #8198, #7394, #4157 ) ;
#7481=DIRECTION ( 'NONE',  ( -1.000000000000000000, -0.000000000000000000, -0.000000000000000000 ) ) ;
#7532=EDGE_CURVE ( 'NONE', #7882, #2911, #5079, .T. ) ;
#7538=CARTESIAN_POINT ( 'NONE',  ( 1.300000000000000044, -0.7390083445627225744, -1.279999999999999138 ) ) ;
#7540=COLOUR_RGB ( '', 0.66274510, 0.83137255, 0.94901961) ;
#7551=CARTESIAN_POINT ( 'NONE',  ( 1.300000000000000044, -0.7390083445627200209, 1.280000000000001137 ) ) ;
#7552=VECTOR ( 'NONE', #9237, 1000.000000000000000 ) ;
#7555=VECTOR ( 'NONE', #5560, 1000.000000000000000 ) ;
#7584=CARTESIAN_POINT ( 'NONE',  ( 1.300000000000000044, -1.478016689125442706, 1.843143693225357538E-15 ) ) ;
#7596=AXIS2_PLACEMENT_3D ( 'NONE', #4660, #1434, #7906 ) ;
#7597=ADVANCED_FACE ( 'NONE', ( #4382 ), #10283, .T. ) ;
#7611=EDGE_CURVE ( 'NONE', #5208, #8384, #7613, .T. ) ;
#7613=CIRCLE ( 'NONE', #1868, 1.280000000000000027 ) ;
#7614=DIRECTION ( 'NONE',  ( -1.000000000000000000, -0.000000000000000000, -0.000000000000000000 ) ) ;
#7655=DIRECTION ( 'NONE',  ( 0.000000000000000000, -0.5000000000000009992, -0.8660254037844380415 ) ) ;
#7665=SHAPE_REPRESENTATION_RELATIONSHIP ( 'NONE' , 'NONE' ,  #7207, #9161 ) ;
#7676=DIRECTION ( 'NONE',  ( -1.000000000000000000, -0.000000000000000000, -0.000000000000000000 ) ) ;
#7685=ORIENTED_EDGE ( 'NONE', *, *, #9134, .F. ) ;
#7691=ORIENTED_EDGE ( 'NONE', *, *, #9984, .T. ) ;
#7694=CARTESIAN_POINT ( 'NONE',  ( 0.000000000000000000, -0.7390083445627225744, -1.279999999999999138 ) ) ;
#7736=ORIENTED_EDGE ( 'NONE', *, *, #3307, .F. ) ;
#7737=EDGE_CURVE ( 'NONE', #2911, #2633, #3115, .T. ) ;
#7745=DIRECTION ( 'NONE',  ( 1.000000000000000000, 0.000000000000000000, 0.000000000000000000 ) ) ;
#7750=DIRECTION ( 'NONE',  ( 0.000000000000000000, 0.000000000000000000, -1.000000000000000000 ) ) ;
#7759=CARTESIAN_POINT ( 'NONE',  ( 3.000000000000000888, 0.000000000000000000, 0.000000000000000000 ) ) ;
#7792=AXIS2_PLACEMENT_3D ( 'NONE', #7992, #3005, #10223 ) ;
#7794=ADVANCED_FACE ( 'NONE', ( #7246 ), #9706, .F. ) ;
#7812=CIRCLE ( 'NONE', #2731, 2.600000000000000089 ) ;
#7813=ORIENTED_EDGE ( 'NONE', *, *, #9146, .F. ) ;
#7825=ORIENTED_EDGE ( 'NONE', *, *, #9453, .T. ) ;
#7833=EDGE_LOOP ( 'NONE', ( #9866, #824, #4274, #1186, #8521 ) ) ;
#7834=LINE ( 'NONE', #9486, #8903 ) ;
#7844=FACE_OUTER_BOUND ( 'NONE', #8529, .T. ) ;
#7847=CIRCLE ( 'NONE', #6486, 1.500000000000000222 ) ;
#7876=AXIS2_PLACEMENT_3D ( 'NONE', #1445, #5467, #356 ) ;
#7882=VERTEX_POINT ( 'NONE', #8682 ) ;
#7888=ORIENTED_EDGE ( 'NONE', *, *, #7532, .F. ) ;
#7902=DIRECTION ( 'NONE',  ( 0.000000000000000000, 0.000000000000000000, 1.000000000000000000 ) ) ;
#7906=DIRECTION ( 'NONE',  ( 0.000000000000000000, 0.000000000000000000, 1.000000000000000000 ) ) ;
#7911=ORIENTED_EDGE ( 'NONE', *, *, #7737, .T. ) ;
#7936=EDGE_LOOP ( 'NONE', ( #4112, #2038, #3230, #1162 ) ) ;
#7946=VERTEX_POINT ( 'NONE', #4914 ) ;
#7955=CARTESIAN_POINT ( 'NONE',  ( 1.300000000000000044, 1.567547902908612085E-16, -1.280000000000000027 ) ) ;
#7966=LINE ( 'NONE', #8022, #5961 ) ;
#7969=SHAPE_DEFINITION_REPRESENTATION ( #9446, #7207 ) ;
#7992=CARTESIAN_POINT ( 'NONE',  ( 11.00000000000000355, 0.000000000000000000, 0.000000000000000000 ) ) ;
#8000=DIRECTION ( 'NONE',  ( 0.000000000000000000, 0.000000000000000000, 1.000000000000000000 ) ) ;
#8012=FACE_OUTER_BOUND ( 'NONE', #2539, .T. ) ;
#8017=DIRECTION ( 'NONE',  ( -0.5000000000000034417, 0.000000000000000000, 0.8660254037844367092 ) ) ;
#8022=CARTESIAN_POINT ( 'NONE',  ( 1.300000000000000044, -0.7390083445627200209, 1.280000000000001137 ) ) ;
#8052=VECTOR ( 'NONE', #9660, 999.9999999999998863 ) ;
#8067=LINE ( 'NONE', #7955, #8052 ) ;
#8089=ORIENTED_EDGE ( 'NONE', *, *, #6029, .T. ) ;
#8093=EDGE_CURVE ( 'NONE', #8610, #7946, #853, .T. ) ;
#8108=PLANE ( 'NONE',  #5793 ) ;
#8112=EDGE_CURVE ( 'NONE', #165, #7946, #510, .T. ) ;
#8157=CONICAL_SURFACE ( 'NONE', #10219, 1.280000000000000027, 1.047197551196593857 ) ;
#8169=ORIENTED_EDGE ( 'NONE', *, *, #1901, .T. ) ;
#8189=CARTESIAN_POINT ( 'NONE',  ( 3.000000000000002665, 3.367778697655221012E-16, -2.750000000000000000 ) ) ;
#8198=CARTESIAN_POINT ( 'NONE',  ( -31.74999999999995737, 0.000000000000000000, 0.000000000000000000 ) ) ;
#8245=PLANE ( 'NONE',  #4573 ) ;
#8261=ORIENTED_EDGE ( 'NONE', *, *, #8093, .F. ) ;
#8286=DIRECTION ( 'NONE',  ( 0.000000000000000000, -0.5000000000000009992, -0.8660254037844380415 ) ) ;
#8290=CIRCLE ( 'NONE', #3869, 1.500000000000000222 ) ;
#8293=EDGE_CURVE ( 'NONE', #6113, #3693, #9584, .T. ) ;
#8297=VERTEX_POINT ( 'NONE', #4742 ) ;
#8343=LINE ( 'NONE', #7538, #7552 ) ;
#8344=FACE_OUTER_BOUND ( 'NONE', #1310, .T. ) ;
#8362=PRESENTATION_STYLE_ASSIGNMENT (( #6702 ) ) ;
#8369=DIRECTION ( 'NONE',  ( 0.000000000000000000, 0.000000000000000000, -1.000000000000000000 ) ) ;
#8371=VERTEX_POINT ( 'NONE', #5843 ) ;
#8375=ADVANCED_FACE ( 'NONE', ( #5688 ), #2520, .F. ) ;
#8384=VERTEX_POINT ( 'NONE', #191 ) ;
#8420=ORIENTED_EDGE ( 'NONE', *, *, #787, .T. ) ;
#8454=ORIENTED_EDGE ( 'NONE', *, *, #10108, .F. ) ;
#8465=FACE_OUTER_BOUND ( 'NONE', #3842, .T. ) ;
#8490=VECTOR ( 'NONE', #2989, 1000.000000000000000 ) ;
#8504=EDGE_CURVE ( 'NONE', #8384, #520, #10155, .T. ) ;
#8521=ORIENTED_EDGE ( 'NONE', *, *, #7014, .T. ) ;
#8529=EDGE_LOOP ( 'NONE', ( #359, #7888, #6400, #1633, #4641 ) ) ;
#8537=VERTEX_POINT ( 'NONE', #4516 ) ;
#8560=AXIS2_PLACEMENT_3D ( 'NONE', #9155, #1685, #6704 ) ;
#8564=EDGE_CURVE ( 'NONE', #798, #8297, #9298, .T. ) ;
#8610=VERTEX_POINT ( 'NONE', #5992 ) ;
#8647=STYLED_ITEM ( 'NONE', ( #3999 ), #1236 ) ;
#8655=AXIS2_PLACEMENT_3D ( 'NONE', #4431, #7676, #4748 ) ;
#8664=FACE_OUTER_BOUND ( 'NONE', #5184, .T. ) ;
#8668=ORIENTED_EDGE ( 'NONE', *, *, #480, .F. ) ;
#8679=EDGE_LOOP ( 'NONE', ( #6386, #2324 ) ) ;
#8682=CARTESIAN_POINT ( 'NONE',  ( 1.300000000000000044, -0.7390083445627200209, 1.280000000000001137 ) ) ;
#8703=VERTEX_POINT ( 'NONE', #3775 ) ;
#8718=CARTESIAN_POINT ( 'NONE',  ( 10.71950000000001424, 0.000000000000000000, 0.000000000000000000 ) ) ;
#8729=TOROIDAL_SURFACE ( 'NONE', #5506, 2.600000000000000089, 0.1499999999999999944 ) ;
#8739=DIRECTION ( 'NONE',  ( 0.000000000000000000, 0.000000000000000000, 1.000000000000000000 ) ) ;
#8757=PRODUCT_CONTEXT ( 'NONE', #4179, 'mechanical' ) ;
#8775=CARTESIAN_POINT ( 'NONE',  ( 1.300000000000000044, 1.478016689125442484, -1.626303258728256651E-15 ) ) ;
#8788=CARTESIAN_POINT ( 'NONE',  ( 0.000000000000000000, -0.7390083445627200209, 1.280000000000001137 ) ) ;
#8798=PLANE ( 'NONE',  #3959 ) ;
#8801=DIRECTION ( 'NONE',  ( -1.000000000000000000, -0.000000000000000000, -0.000000000000000000 ) ) ;
#8806=CARTESIAN_POINT ( 'NONE',  ( 11.00000000000000355, 0.000000000000000000, 0.000000000000000000 ) ) ;
#8824=FACE_OUTER_BOUND ( 'NONE', #3108, .T. ) ;
#8831=AXIS2_PLACEMENT_3D ( 'NONE', #494, #2143, #5941 ) ;
#8833=CARTESIAN_POINT ( 'NONE',  ( 0.000000000000000000, 0.7390083445627193548, -1.280000000000000693 ) ) ;
#8846=DIRECTION ( 'NONE',  ( 0.000000000000000000, 1.000000000000000000, -1.320393690296331133E-15 ) ) ;
#8854=DIRECTION ( 'NONE',  ( 1.000000000000000000, 0.000000000000000000, 0.000000000000000000 ) ) ;
#8870=CARTESIAN_POINT ( 'NONE',  ( 0.000000000000000000, 1.478016689125442484, -1.626303258728256651E-15 ) ) ;
#8871=DIRECTION ( 'NONE',  ( 1.000000000000000000, 0.000000000000000000, 0.000000000000000000 ) ) ;
#8880=ORIENTED_EDGE ( 'NONE', *, *, #2682, .T. ) ;
#8903=VECTOR ( 'NONE', #786, 1000.000000000000000 ) ;
#8906=ORIENTED_EDGE ( 'NONE', *, *, #5708, .F. ) ;
#8913=LINE ( 'NONE', #6406, #6577 ) ;
#8933=ORIENTED_EDGE ( 'NONE', *, *, #6029, .F. ) ;
#8945=VERTEX_POINT ( 'NONE', #1111 ) ;
#8951=ADVANCED_FACE ( 'NONE', ( #319 ), #8157, .F. ) ;
#8959=DIRECTION ( 'NONE',  ( -1.000000000000000000, -0.000000000000000000, -0.000000000000000000 ) ) ;
#8974=VECTOR ( 'NONE', #2250, 1000.000000000000227 ) ;
#8979=DIRECTION ( 'NONE',  ( 0.000000000000000000, -1.026972870230479989E-15, -1.000000000000000000 ) ) ;
#8987=DIRECTION ( 'NONE',  ( -1.000000000000000000, -0.000000000000000000, -0.000000000000000000 ) ) ;
#9027=AXIS2_PLACEMENT_3D ( 'NONE', #6396, #3222, #8739 ) ;
#9034=SURFACE_SIDE_STYLE ('',( #77 ) ) ;
#9038=EDGE_LOOP ( 'NONE', ( #7736, #9964, #8261, #10162 ) ) ;
#9056=EDGE_LOOP ( 'NONE', ( #4926, #454 ) ) ;
#9076=ORIENTED_EDGE ( 'NONE', *, *, #1943, .T. ) ;
#9093=ADVANCED_FACE ( 'NONE', ( #10133 ), #1216, .F. ) ;
#9122=ORIENTED_EDGE ( 'NONE', *, *, #8504, .F. ) ;
#9124=CARTESIAN_POINT ( 'NONE',  ( 0.1499999999999973577, 0.000000000000000000, 0.000000000000000000 ) ) ;
#9134=EDGE_CURVE ( 'NONE', #8297, #4172, #5445, .T. ) ;
#9138=CIRCLE ( 'NONE', #7792, 1.219500000000000028 ) ;
#9146=EDGE_CURVE ( 'NONE', #7882, #8384, #6926, .T. ) ;
#9155=CARTESIAN_POINT ( 'NONE',  ( 3.099999999999998757, 1.959434878635765477E-16, 1.600000000000000311 ) ) ;
#9161=ADVANCED_BREP_SHAPE_REPRESENTATION ( '', ( #1236, #2101 ), #1104 ) ;
#9173=DIRECTION ( 'NONE',  ( -1.000000000000000000, -0.000000000000000000, -0.000000000000000000 ) ) ;
#9185=DIRECTION ( 'NONE',  ( 0.000000000000000000, 0.000000000000000000, -1.000000000000000000 ) ) ;
#9227=ORIENTED_EDGE ( 'NONE', *, *, #3734, .T. ) ;
#9228=TOROIDAL_SURFACE ( 'NONE', #6337, 1.600000000000000311, 0.1000000000000000056 ) ;
#9237=DIRECTION ( 'NONE',  ( -1.000000000000000000, -0.000000000000000000, -0.000000000000000000 ) ) ;
#9268=EDGE_CURVE ( 'NONE', #8703, #65, #3970, .T. ) ;
#9270=DIRECTION ( 'NONE',  ( 0.000000000000000000, 0.000000000000000000, -1.000000000000000000 ) ) ;
#9298=LINE ( 'NONE', #448, #4920 ) ;
#9318=DIRECTION ( 'NONE',  ( -1.000000000000000000, 0.000000000000000000, -0.000000000000000000 ) ) ;
#9325=DIRECTION ( 'NONE',  ( -1.000000000000000000, -0.000000000000000000, -0.000000000000000000 ) ) ;
#9332=CARTESIAN_POINT ( 'NONE',  ( 1.300000000000000044, 1.478016689125442484, -1.626303258728256651E-15 ) ) ;
#9359=CARTESIAN_POINT ( 'NONE',  ( 1.300000000000000044, 1.478016689125442484, -1.626303258728256651E-15 ) ) ;
#9367=VECTOR ( 'NONE', #2118, 1000.000000000000114 ) ;
#9375=PRODUCT_DEFINITION_CONTEXT ( 'detailed design', #54, 'design' ) ;
#9382=DIRECTION ( 'NONE',  ( 0.000000000000000000, 0.000000000000000000, -1.000000000000000000 ) ) ;
#9389=ADVANCED_FACE ( 'NONE', ( #7197 ), #8108, .T. ) ;
#9407=CARTESIAN_POINT ( 'NONE',  ( 11.00000000000000355, 0.000000000000000000, 1.219500000000000028 ) ) ;
#9414=CIRCLE ( 'NONE', #783, 2.750000000000000000 ) ;
#9423=AXIS2_PLACEMENT_3D ( 'NONE', #6836, #10093, #7750 ) ;
#9446=PRODUCT_DEFINITION_SHAPE ( 'NONE', 'NONE',  #4567 ) ;
#9453=EDGE_CURVE ( 'NONE', #2420, #165, #2932, .T. ) ;
#9457=ORIENTED_EDGE ( 'NONE', *, *, #1260, .T. ) ;
#9465=LINE ( 'NONE', #2304, #8974 ) ;
#9471=DIRECTION ( 'NONE',  ( 0.000000000000000000, 0.000000000000000000, 1.000000000000000000 ) ) ;
#9486=CARTESIAN_POINT ( 'NONE',  ( 1.300000000000000044, 0.7390083445627193548, -1.280000000000000693 ) ) ;
#9498=DIRECTION ( 'NONE',  ( -0.7071067811865335839, 8.659560562355102956E-17, -0.7071067811865614505 ) ) ;
#9504=EDGE_CURVE ( 'NONE', #8537, #3139, #10404, .T. ) ;
#9505=CARTESIAN_POINT ( 'NONE',  ( 0.000000000000000000, 0.7390083445627193548, -1.280000000000000693 ) ) ;
#9524=PLANE ( 'NONE',  #1706 ) ;
#9549=VECTOR ( 'NONE', #1725, 1000.000000000000000 ) ;
#9553=EDGE_LOOP ( 'NONE', ( #9566, #9122, #7199 ) ) ;
#9565=CARTESIAN_POINT ( 'NONE',  ( -31.74999999999995737, 1.836970198721030181E-16, -1.500000000000000222 ) ) ;
#9566=ORIENTED_EDGE ( 'NONE', *, *, #5334, .F. ) ;
#9576=AXIS2_PLACEMENT_3D ( 'NONE', #10230, #2959, #9270 ) ;
#9583=VECTOR ( 'NONE', #623, 1000.000000000000000 ) ;
#9584=LINE ( 'NONE', #8775, #354 ) ;
#9587=DIRECTION ( 'NONE',  ( -1.000000000000000000, -0.000000000000000000, -0.000000000000000000 ) ) ;
#9607=FACE_OUTER_BOUND ( 'NONE', #5417, .T. ) ;
#9620=ORIENTED_EDGE ( 'NONE', *, *, #3734, .F. ) ;
#9627=FACE_OUTER_BOUND ( 'NONE', #9553, .T. ) ;
#9649=DIRECTION ( 'NONE',  ( 1.000000000000000000, 0.000000000000000000, 0.000000000000000000 ) ) ;
#9660=DIRECTION ( 'NONE',  ( -0.5000000000000034417, 1.060575238724904696E-16, -0.8660254037844367092 ) ) ;
#9681=CARTESIAN_POINT ( 'NONE',  ( 0.1499999999999973577, 0.000000000000000000, 0.000000000000000000 ) ) ;
#9692=AXIS2_PLACEMENT_3D ( 'NONE', #7759, #10208, #10103 ) ;
#9704=( NAMED_UNIT ( * ) PLANE_ANGLE_UNIT ( ) SI_UNIT ( $, .RADIAN. ) );
#9706=PLANE ( 'NONE',  #2033 ) ;
#9724=CARTESIAN_POINT ( 'NONE',  ( 1.300000000000000044, 0.000000000000000000, 0.000000000000000000 ) ) ;
#9739=ORIENTED_EDGE ( 'NONE', *, *, #4908, .F. ) ;
#9751=( GEOMETRIC_REPRESENTATION_CONTEXT ( 3 ) GLOBAL_UNCERTAINTY_ASSIGNED_CONTEXT ( ( #6917 ) ) GLOBAL_UNIT_ASSIGNED_CONTEXT ( ( #251, #1091, #3628 ) ) REPRESENTATION_CONTEXT ( 'NONE', 'WORKASPACE' ) );
#9754=CONICAL_SURFACE ( 'NONE', #7876, 1.219500000000000028, 0.7853981633974680410 ) ;
#9762=EDGE_CURVE ( 'NONE', #7181, #6915, #9787, .T. ) ;
#9787=LINE ( 'NONE', #3357, #9549 ) ;
#9824=VECTOR ( 'NONE', #7481, 1000.000000000000000 ) ;
#9843=EDGE_LOOP ( 'NONE', ( #7299, #1090, #3795, #5966 ) ) ;
#9847=PLANE ( 'NONE',  #532 ) ;
#9866=ORIENTED_EDGE ( 'NONE', *, *, #6801, .F. ) ;
#9882=DIRECTION ( 'NONE',  ( 0.000000000000000000, 0.000000000000000000, 1.000000000000000000 ) ) ;
#9916=ORIENTED_EDGE ( 'NONE', *, *, #4908, .T. ) ;
#9918=CONICAL_SURFACE ( 'NONE', #7365, 1.280000000000000027, 1.047197551196593857 ) ;
#9925=CARTESIAN_POINT ( 'NONE',  ( 1.300000000000000044, -1.314525273895014473E-15, -1.280000000000000027 ) ) ;
#9934=VECTOR ( 'NONE', #868, 1000.000000000000114 ) ;
#9964=ORIENTED_EDGE ( 'NONE', *, *, #8112, .T. ) ;
#9980=EDGE_CURVE ( 'NONE', #8371, #3693, #7966, .T. ) ;
#9984=EDGE_CURVE ( 'NONE', #3139, #6004, #3873, .T. ) ;
#9986=PLANE ( 'NONE',  #6185 ) ;
#10009=ORIENTED_EDGE ( 'NONE', *, *, #654, .F. ) ;
#10017=CARTESIAN_POINT ( 'NONE',  ( 0.000000000000000000, 0.000000000000000000, 0.000000000000000000 ) ) ;
#10018=ORIENTED_EDGE ( 'NONE', *, *, #654, .T. ) ;
#10023=ORIENTED_EDGE ( 'NONE', *, *, #8293, .T. ) ;
#10079=EDGE_CURVE ( 'NONE', #8384, #8371, #1078, .T. ) ;
#10093=DIRECTION ( 'NONE',  ( 0.000000000000000000, -1.000000000000000000, 0.000000000000000000 ) ) ;
#10103=DIRECTION ( 'NONE',  ( 0.000000000000000000, 0.000000000000000000, -1.000000000000000000 ) ) ;
#10108=EDGE_CURVE ( 'NONE', #6004, #4105, #7847, .T. ) ;
#10113=SURFACE_STYLE_FILL_AREA ( #1044 ) ;
#10118=DIRECTION ( 'NONE',  ( -0.000000000000000000, 1.000000000000000000, 1.224646799147353207E-16 ) ) ;
#10133=FACE_OUTER_BOUND ( 'NONE', #3958, .T. ) ;
#10134=FACE_OUTER_BOUND ( 'NONE', #10178, .T. ) ;
#10148=EDGE_CURVE ( 'NONE', #7882, #8371, #7377, .T. ) ;
#10151=DIRECTION ( 'NONE',  ( 0.000000000000000000, 0.4999999999999991673, -0.8660254037844391517 ) ) ;
#10152=TOROIDAL_SURFACE ( 'NONE', #5563, 1.600000000000000311, 0.1000000000000000056 ) ;
#10155=LINE ( 'NONE', #5157, #7470 ) ;
#10162=ORIENTED_EDGE ( 'NONE', *, *, #3649, .F. ) ;
#10175=AXIS2_PLACEMENT_3D ( 'NONE', #6007, #10118, #6864 ) ;
#10178=EDGE_LOOP ( 'NONE', ( #8933, #1575, #6052, #4870 ) ) ;
#10190=EDGE_CURVE ( 'NONE', #2911, #5053, #6467, .T. ) ;
#10208=DIRECTION ( 'NONE',  ( -1.000000000000000000, -0.000000000000000000, -0.000000000000000000 ) ) ;
#10219=AXIS2_PLACEMENT_3D ( 'NONE', #3351, #813, #6578 ) ;
#10223=DIRECTION ( 'NONE',  ( 0.000000000000000000, 0.000000000000000000, 1.000000000000000000 ) ) ;
#10230=CARTESIAN_POINT ( 'NONE',  ( 3.099999999999998757, 0.000000000000000000, 0.000000000000000000 ) ) ;
#10259=CARTESIAN_POINT ( 'NONE',  ( 10.71950000000001424, 1.836970198721030181E-16, -1.500000000000000222 ) ) ;
#10268=ADVANCED_FACE ( 'NONE', ( #432 ), #1120, .F. ) ;
#10283=CYLINDRICAL_SURFACE ( 'NONE', #6425, 2.750000000000000000 ) ;
#10284=ORIENTED_EDGE ( 'NONE', *, *, #1304, .F. ) ;
#10294=CARTESIAN_POINT ( 'NONE',  ( -31.74999999999995737, 0.000000000000000000, 0.000000000000000000 ) ) ;
#10314=VECTOR ( 'NONE', #8017, 999.9999999999998863 ) ;
#10337=CARTESIAN_POINT ( 'NONE',  ( 1.300000000000000044, 1.478016689125442484, -1.626303258728256651E-15 ) ) ;
#10342=ORIENTED_EDGE ( 'NONE', *, *, #6196, .T. ) ;
#10348=DIRECTION ( 'NONE',  ( 0.000000000000000000, 0.5000000000000009992, 0.8660254037844380415 ) ) ;
#10382=VERTEX_POINT ( 'NONE', #7694 ) ;
#10404=LINE ( 'NONE', #3756, #7153 ) ;
#10420=PLANE ( 'NONE',  #7033 ) ;
#10443=DIRECTION ( 'NONE',  ( 0.000000000000000000, 0.000000000000000000, 1.000000000000000000 ) ) ;
#10467=CARTESIAN_POINT ( 'NONE',  ( 2.039008344562727615, -1.214068345727601445E-18, 0.000000000000000000 ) ) ;
#10482=PLANE ( 'NONE',  #1859 ) ;
#10485=ADVANCED_FACE ( 'NONE', ( #7844 ), #8798, .T. ) ;
ENDSEC;
END-ISO-10303-21;
